ISO-10303-21;
HEADER;
/* Generated by software containing ST-Developer
 * from STEP Tools, Inc. (www.steptools.com) 
 */

FILE_DESCRIPTION(
/* description */ ('Torsion-spring ratchet demonstrator'),
/* implementation_level */ '2;1');

FILE_NAME(
/* name */ 'M5x14 Cap Screw.step',
/* time_stamp */ '2026-10-29T17:29:17-07:00',
/* author */ (''),
/* organization */ (''),
/* preprocessor_version */ 'ST-DEVELOPER v20.2',
/* originating_system */ 'Autodesk Translation Framework v15.17.0.0',
/* authorisation */ '');

FILE_SCHEMA (('AUTOMOTIVE_DESIGN { 1 0 10303 214 3 1 1 }'));
ENDSEC;

DATA;
#10=MECHANICAL_DESIGN_GEOMETRIC_PRESENTATION_REPRESENTATION('',(#305),#11258);
#14=ORIENTED_CLOSED_SHELL('',*,#5176,.F.);
#16=BREP_WITH_VOIDS('Body1',#5177,(#14));
#190=CONICAL_SURFACE('',#5827,0.4,0.785398163397448);
#191=CONICAL_SURFACE('',#5831,0.41,0.785398163397448);
#192=CONICAL_SURFACE('',#5835,0.26,0.463647609000806);
#249=SHAPE_REPRESENTATION_RELATIONSHIP('SRR','None',#11376,#273);
#273=ADVANCED_BREP_SHAPE_REPRESENTATION('',(#16),#11246);
#305=STYLED_ITEM('',(#11591),#16);
#418=FACE_BOUND('',#1170,.T.);
#506=PLANE('',#5815);
#507=PLANE('',#5816);
#508=PLANE('',#5817);
#509=PLANE('',#5818);
#510=PLANE('',#5819);
#511=PLANE('',#5820);
#512=PLANE('',#5821);
#513=PLANE('',#5822);
#514=PLANE('',#5823);
#515=PLANE('',#5825);
#516=PLANE('',#5833);
#778=FACE_OUTER_BOUND('',#1156,.T.);
#779=FACE_OUTER_BOUND('',#1157,.T.);
#780=FACE_OUTER_BOUND('',#1158,.T.);
#781=FACE_OUTER_BOUND('',#1159,.T.);
#782=FACE_OUTER_BOUND('',#1160,.T.);
#783=FACE_OUTER_BOUND('',#1161,.T.);
#784=FACE_OUTER_BOUND('',#1162,.T.);
#785=FACE_OUTER_BOUND('',#1163,.T.);
#786=FACE_OUTER_BOUND('',#1164,.T.);
#787=FACE_OUTER_BOUND('',#1165,.T.);
#788=FACE_OUTER_BOUND('',#1166,.T.);
#789=FACE_OUTER_BOUND('',#1167,.T.);
#790=FACE_OUTER_BOUND('',#1168,.T.);
#791=FACE_OUTER_BOUND('',#1169,.T.);
#792=FACE_OUTER_BOUND('',#1171,.T.);
#793=FACE_OUTER_BOUND('',#1172,.T.);
#1156=EDGE_LOOP('',(#4074,#4075,#4076,#4077));
#1157=EDGE_LOOP('',(#4078,#4079,#4080,#4081));
#1158=EDGE_LOOP('',(#4082,#4083,#4084,#4085));
#1159=EDGE_LOOP('',(#4086,#4087,#4088,#4089));
#1160=EDGE_LOOP('',(#4090,#4091,#4092,#4093));
#1161=EDGE_LOOP('',(#4094,#4095,#4096,#4097));
#1162=EDGE_LOOP('',(#4098,#4099,#4100,#4101,#4102,#4103));
#1163=EDGE_LOOP('',(#4104,#4105,#4106,#4107,#4108,#4109));
#1164=EDGE_LOOP('',(#4110));
#1165=EDGE_LOOP('',(#4111));
#1166=EDGE_LOOP('',(#4112,#4113,#4114,#4115));
#1167=EDGE_LOOP('',(#4116,#4117,#4118,#4119));
#1168=EDGE_LOOP('',(#4120,#4121,#4122,#4123));
#1169=EDGE_LOOP('',(#4124));
#1170=EDGE_LOOP('',(#4125));
#1171=EDGE_LOOP('',(#4126,#4127,#4128,#4129));
#1172=EDGE_LOOP('',(#4130,#4131,#4132,#4133));
#1435=LINE('',#8798,#1818);
#1436=LINE('',#8800,#1819);
#1437=LINE('',#8802,#1820);
#1438=LINE('',#8803,#1821);
#1439=LINE('',#8806,#1822);
#1440=LINE('',#8808,#1823);
#1441=LINE('',#8809,#1824);
#1442=LINE('',#8812,#1825);
#1443=LINE('',#8814,#1826);
#1444=LINE('',#8815,#1827);
#1445=LINE('',#8818,#1828);
#1446=LINE('',#8820,#1829);
#1447=LINE('',#8821,#1830);
#1448=LINE('',#8824,#1831);
#1449=LINE('',#8826,#1832);
#1450=LINE('',#8827,#1833);
#1451=LINE('',#8829,#1834);
#1452=LINE('',#8830,#1835);
#1453=LINE('',#8842,#1836);
#1454=LINE('',#8846,#1837);
#1455=LINE('',#8850,#1838);
#1456=LINE('',#8857,#1839);
#1457=LINE('',#8859,#1840);
#1818=VECTOR('',#6902,1.);
#1819=VECTOR('',#6903,1.);
#1820=VECTOR('',#6904,1.);
#1821=VECTOR('',#6905,1.);
#1822=VECTOR('',#6908,1.);
#1823=VECTOR('',#6909,1.);
#1824=VECTOR('',#6910,1.);
#1825=VECTOR('',#6913,1.);
#1826=VECTOR('',#6914,1.);
#1827=VECTOR('',#6915,1.);
#1828=VECTOR('',#6918,1.);
#1829=VECTOR('',#6919,1.);
#1830=VECTOR('',#6920,1.);
#1831=VECTOR('',#6923,1.);
#1832=VECTOR('',#6924,1.);
#1833=VECTOR('',#6925,1.);
#1834=VECTOR('',#6928,1.);
#1835=VECTOR('',#6929,1.);
#1836=VECTOR('',#6946,0.4);
#1837=VECTOR('',#6951,0.425);
#1838=VECTOR('',#6956,0.41);
#1839=VECTOR('',#6965,0.26);
#1840=VECTOR('',#6968,0.25);
#2275=CIRCLE('',#5824,0.24505);
#2276=CIRCLE('',#5826,0.375);
#2277=CIRCLE('',#5828,0.425);
#2278=CIRCLE('',#5830,0.425);
#2279=CIRCLE('',#5832,0.395);
#2280=CIRCLE('',#5834,0.27);
#2281=CIRCLE('',#5836,0.24505);
#2555=VERTEX_POINT('',#8796);
#2556=VERTEX_POINT('',#8797);
#2557=VERTEX_POINT('',#8799);
#2558=VERTEX_POINT('',#8801);
#2559=VERTEX_POINT('',#8805);
#2560=VERTEX_POINT('',#8807);
#2561=VERTEX_POINT('',#8811);
#2562=VERTEX_POINT('',#8813);
#2563=VERTEX_POINT('',#8817);
#2564=VERTEX_POINT('',#8819);
#2565=VERTEX_POINT('',#8823);
#2566=VERTEX_POINT('',#8825);
#2567=VERTEX_POINT('',#8834);
#2568=VERTEX_POINT('',#8837);
#2569=VERTEX_POINT('',#8840);
#2570=VERTEX_POINT('',#8844);
#2571=VERTEX_POINT('',#8848);
#2572=VERTEX_POINT('',#8852);
#2573=VERTEX_POINT('',#8855);
#3097=EDGE_CURVE('',#2555,#2556,#1435,.T.);
#3098=EDGE_CURVE('',#2556,#2557,#1436,.T.);
#3099=EDGE_CURVE('',#2557,#2558,#1437,.T.);
#3100=EDGE_CURVE('',#2555,#2558,#1438,.T.);
#3101=EDGE_CURVE('',#2556,#2559,#1439,.T.);
#3102=EDGE_CURVE('',#2559,#2560,#1440,.T.);
#3103=EDGE_CURVE('',#2560,#2557,#1441,.T.);
#3104=EDGE_CURVE('',#2559,#2561,#1442,.T.);
#3105=EDGE_CURVE('',#2561,#2562,#1443,.T.);
#3106=EDGE_CURVE('',#2562,#2560,#1444,.T.);
#3107=EDGE_CURVE('',#2561,#2563,#1445,.T.);
#3108=EDGE_CURVE('',#2563,#2564,#1446,.T.);
#3109=EDGE_CURVE('',#2564,#2562,#1447,.T.);
#3110=EDGE_CURVE('',#2563,#2565,#1448,.T.);
#3111=EDGE_CURVE('',#2565,#2566,#1449,.T.);
#3112=EDGE_CURVE('',#2566,#2564,#1450,.T.);
#3113=EDGE_CURVE('',#2565,#2555,#1451,.T.);
#3114=EDGE_CURVE('',#2558,#2566,#1452,.T.);
#3115=EDGE_CURVE('',#2567,#2567,#2275,.T.);
#3116=EDGE_CURVE('',#2568,#2568,#2276,.T.);
#3117=EDGE_CURVE('',#2569,#2569,#2277,.T.);
#3118=EDGE_CURVE('',#2569,#2568,#1453,.T.);
#3119=EDGE_CURVE('',#2570,#2570,#2278,.T.);
#3120=EDGE_CURVE('',#2570,#2569,#1454,.T.);
#3121=EDGE_CURVE('',#2571,#2571,#2279,.T.);
#3122=EDGE_CURVE('',#2571,#2570,#1455,.T.);
#3123=EDGE_CURVE('',#2572,#2572,#2280,.T.);
#3124=EDGE_CURVE('',#2573,#2573,#2281,.F.);
#3125=EDGE_CURVE('',#2573,#2572,#1456,.T.);
#3126=EDGE_CURVE('',#2567,#2573,#1457,.T.);
#4074=ORIENTED_EDGE('',*,*,#3097,.T.);
#4075=ORIENTED_EDGE('',*,*,#3098,.T.);
#4076=ORIENTED_EDGE('',*,*,#3099,.T.);
#4077=ORIENTED_EDGE('',*,*,#3100,.F.);
#4078=ORIENTED_EDGE('',*,*,#3101,.T.);
#4079=ORIENTED_EDGE('',*,*,#3102,.T.);
#4080=ORIENTED_EDGE('',*,*,#3103,.T.);
#4081=ORIENTED_EDGE('',*,*,#3098,.F.);
#4082=ORIENTED_EDGE('',*,*,#3104,.T.);
#4083=ORIENTED_EDGE('',*,*,#3105,.T.);
#4084=ORIENTED_EDGE('',*,*,#3106,.T.);
#4085=ORIENTED_EDGE('',*,*,#3102,.F.);
#4086=ORIENTED_EDGE('',*,*,#3107,.T.);
#4087=ORIENTED_EDGE('',*,*,#3108,.T.);
#4088=ORIENTED_EDGE('',*,*,#3109,.T.);
#4089=ORIENTED_EDGE('',*,*,#3105,.F.);
#4090=ORIENTED_EDGE('',*,*,#3110,.T.);
#4091=ORIENTED_EDGE('',*,*,#3111,.T.);
#4092=ORIENTED_EDGE('',*,*,#3112,.T.);
#4093=ORIENTED_EDGE('',*,*,#3108,.F.);
#4094=ORIENTED_EDGE('',*,*,#3113,.T.);
#4095=ORIENTED_EDGE('',*,*,#3100,.T.);
#4096=ORIENTED_EDGE('',*,*,#3114,.T.);
#4097=ORIENTED_EDGE('',*,*,#3111,.F.);
#4098=ORIENTED_EDGE('',*,*,#3113,.F.);
#4099=ORIENTED_EDGE('',*,*,#3110,.F.);
#4100=ORIENTED_EDGE('',*,*,#3107,.F.);
#4101=ORIENTED_EDGE('',*,*,#3104,.F.);
#4102=ORIENTED_EDGE('',*,*,#3101,.F.);
#4103=ORIENTED_EDGE('',*,*,#3097,.F.);
#4104=ORIENTED_EDGE('',*,*,#3114,.F.);
#4105=ORIENTED_EDGE('',*,*,#3099,.F.);
#4106=ORIENTED_EDGE('',*,*,#3103,.F.);
#4107=ORIENTED_EDGE('',*,*,#3106,.F.);
#4108=ORIENTED_EDGE('',*,*,#3109,.F.);
#4109=ORIENTED_EDGE('',*,*,#3112,.F.);
#4110=ORIENTED_EDGE('',*,*,#3115,.F.);
#4111=ORIENTED_EDGE('',*,*,#3116,.F.);
#4112=ORIENTED_EDGE('',*,*,#3117,.F.);
#4113=ORIENTED_EDGE('',*,*,#3118,.T.);
#4114=ORIENTED_EDGE('',*,*,#3116,.T.);
#4115=ORIENTED_EDGE('',*,*,#3118,.F.);
#4116=ORIENTED_EDGE('',*,*,#3119,.F.);
#4117=ORIENTED_EDGE('',*,*,#3120,.T.);
#4118=ORIENTED_EDGE('',*,*,#3117,.T.);
#4119=ORIENTED_EDGE('',*,*,#3120,.F.);
#4120=ORIENTED_EDGE('',*,*,#3121,.F.);
#4121=ORIENTED_EDGE('',*,*,#3122,.T.);
#4122=ORIENTED_EDGE('',*,*,#3119,.T.);
#4123=ORIENTED_EDGE('',*,*,#3122,.F.);
#4124=ORIENTED_EDGE('',*,*,#3121,.T.);
#4125=ORIENTED_EDGE('',*,*,#3123,.F.);
#4126=ORIENTED_EDGE('',*,*,#3124,.F.);
#4127=ORIENTED_EDGE('',*,*,#3125,.T.);
#4128=ORIENTED_EDGE('',*,*,#3123,.T.);
#4129=ORIENTED_EDGE('',*,*,#3125,.F.);
#4130=ORIENTED_EDGE('',*,*,#3115,.T.);
#4131=ORIENTED_EDGE('',*,*,#3126,.T.);
#4132=ORIENTED_EDGE('',*,*,#3124,.T.);
#4133=ORIENTED_EDGE('',*,*,#3126,.F.);
#4828=CYLINDRICAL_SURFACE('',#5829,0.425);
#4829=CYLINDRICAL_SURFACE('',#5837,0.24505);
#5004=ADVANCED_FACE('',(#778),#506,.F.);
#5005=ADVANCED_FACE('',(#779),#507,.F.);
#5006=ADVANCED_FACE('',(#780),#508,.F.);
#5007=ADVANCED_FACE('',(#781),#509,.F.);
#5008=ADVANCED_FACE('',(#782),#510,.F.);
#5009=ADVANCED_FACE('',(#783),#511,.F.);
#5010=ADVANCED_FACE('',(#784),#512,.F.);
#5011=ADVANCED_FACE('',(#785),#513,.F.);
#5012=ADVANCED_FACE('',(#786),#514,.F.);
#5013=ADVANCED_FACE('',(#787),#515,.T.);
#5014=ADVANCED_FACE('',(#788),#190,.T.);
#5015=ADVANCED_FACE('',(#789),#4828,.T.);
#5016=ADVANCED_FACE('',(#790),#191,.T.);
#5017=ADVANCED_FACE('',(#791,#418),#516,.T.);
#5018=ADVANCED_FACE('',(#792),#192,.T.);
#5019=ADVANCED_FACE('',(#793),#4829,.T.);
#5176=CLOSED_SHELL('',(#5004,#5005,#5006,#5007,#5008,#5009,#5010,#5011));
#5177=CLOSED_SHELL('',(#5012,#5013,#5014,#5015,#5016,#5017,#5018,#5019));
#5814=AXIS2_PLACEMENT_3D('',#8794,#6898,#6899);
#5815=AXIS2_PLACEMENT_3D('',#8795,#6900,#6901);
#5816=AXIS2_PLACEMENT_3D('',#8804,#6906,#6907);
#5817=AXIS2_PLACEMENT_3D('',#8810,#6911,#6912);
#5818=AXIS2_PLACEMENT_3D('',#8816,#6916,#6917);
#5819=AXIS2_PLACEMENT_3D('',#8822,#6921,#6922);
#5820=AXIS2_PLACEMENT_3D('',#8828,#6926,#6927);
#5821=AXIS2_PLACEMENT_3D('',#8831,#6930,#6931);
#5822=AXIS2_PLACEMENT_3D('',#8832,#6932,#6933);
#5823=AXIS2_PLACEMENT_3D('',#8833,#6934,#6935);
#5824=AXIS2_PLACEMENT_3D('',#8835,#6936,#6937);
#5825=AXIS2_PLACEMENT_3D('',#8836,#6938,#6939);
#5826=AXIS2_PLACEMENT_3D('',#8838,#6940,#6941);
#5827=AXIS2_PLACEMENT_3D('',#8839,#6942,#6943);
#5828=AXIS2_PLACEMENT_3D('',#8841,#6944,#6945);
#5829=AXIS2_PLACEMENT_3D('',#8843,#6947,#6948);
#5830=AXIS2_PLACEMENT_3D('',#8845,#6949,#6950);
#5831=AXIS2_PLACEMENT_3D('',#8847,#6952,#6953);
#5832=AXIS2_PLACEMENT_3D('',#8849,#6954,#6955);
#5833=AXIS2_PLACEMENT_3D('',#8851,#6957,#6958);
#5834=AXIS2_PLACEMENT_3D('',#8853,#6959,#6960);
#5835=AXIS2_PLACEMENT_3D('',#8854,#6961,#6962);
#5836=AXIS2_PLACEMENT_3D('',#8856,#6963,#6964);
#5837=AXIS2_PLACEMENT_3D('',#8858,#6966,#6967);
#6898=DIRECTION('axis',(0.,0.,1.));
#6899=DIRECTION('refdir',(1.,0.,0.));
#6900=DIRECTION('center_axis',(0.866025403784439,0.,-0.5));
#6901=DIRECTION('ref_axis',(0.5,0.,0.866025403784439));
#6902=DIRECTION('',(-0.5,0.,-0.866025403784439));
#6903=DIRECTION('',(0.,-1.,0.));
#6904=DIRECTION('',(0.5,0.,0.866025403784439));
#6905=DIRECTION('',(0.,-1.,0.));
#6906=DIRECTION('center_axis',(1.20185167898973E-16,0.,-1.));
#6907=DIRECTION('ref_axis',(1.,0.,1.20185167898973E-16));
#6908=DIRECTION('',(-1.,0.,-1.20185167898973E-16));
#6909=DIRECTION('',(0.,-1.,0.));
#6910=DIRECTION('',(1.,0.,1.20185167898973E-16));
#6911=DIRECTION('center_axis',(-0.866025403784439,0.,-0.5));
#6912=DIRECTION('ref_axis',(0.5,0.,-0.866025403784439));
#6913=DIRECTION('',(-0.5,0.,0.866025403784439));
#6914=DIRECTION('',(0.,-1.,0.));
#6915=DIRECTION('',(0.5,0.,-0.866025403784439));
#6916=DIRECTION('center_axis',(-0.866025403784439,0.,0.5));
#6917=DIRECTION('ref_axis',(-0.5,0.,-0.866025403784439));
#6918=DIRECTION('',(0.5,0.,0.866025403784439));
#6919=DIRECTION('',(0.,-1.,0.));
#6920=DIRECTION('',(-0.5,0.,-0.866025403784439));
#6921=DIRECTION('center_axis',(-2.40370335797945E-16,0.,1.));
#6922=DIRECTION('ref_axis',(-1.,0.,-2.40370335797945E-16));
#6923=DIRECTION('',(1.,0.,2.40370335797945E-16));
#6924=DIRECTION('',(0.,-1.,0.));
#6925=DIRECTION('',(-1.,0.,-2.40370335797945E-16));
#6926=DIRECTION('center_axis',(0.866025403784439,0.,0.5));
#6927=DIRECTION('ref_axis',(-0.5,0.,0.866025403784439));
#6928=DIRECTION('',(0.5,0.,-0.866025403784439));
#6929=DIRECTION('',(-0.5,0.,0.866025403784439));
#6930=DIRECTION('center_axis',(0.,1.,0.));
#6931=DIRECTION('ref_axis',(1.,0.,0.));
#6932=DIRECTION('center_axis',(0.,-1.,0.));
#6933=DIRECTION('ref_axis',(0.,0.,-1.));
#6934=DIRECTION('center_axis',(0.,1.,0.));
#6935=DIRECTION('ref_axis',(1.,0.,0.));
#6936=DIRECTION('center_axis',(0.,1.,0.));
#6937=DIRECTION('ref_axis',(1.,0.,0.));
#6938=DIRECTION('center_axis',(0.,1.,0.));
#6939=DIRECTION('ref_axis',(0.,0.,1.));
#6940=DIRECTION('center_axis',(0.,-1.,0.));
#6941=DIRECTION('ref_axis',(1.,0.,0.));
#6942=DIRECTION('center_axis',(0.,-1.,0.));
#6943=DIRECTION('ref_axis',(1.,0.,0.));
#6944=DIRECTION('center_axis',(0.,-1.,0.));
#6945=DIRECTION('ref_axis',(1.,0.,0.));
#6946=DIRECTION('',(0.707106781186548,0.707106781186547,8.65956056235493E-17));
#6947=DIRECTION('center_axis',(0.,-1.,0.));
#6948=DIRECTION('ref_axis',(1.,0.,0.));
#6949=DIRECTION('center_axis',(0.,-1.,0.));
#6950=DIRECTION('ref_axis',(1.,0.,0.));
#6951=DIRECTION('',(0.,1.,0.));
#6952=DIRECTION('center_axis',(0.,1.,0.));
#6953=DIRECTION('ref_axis',(1.,0.,0.));
#6954=DIRECTION('center_axis',(0.,-1.,0.));
#6955=DIRECTION('ref_axis',(1.,0.,0.));
#6956=DIRECTION('',(-0.707106781186547,0.707106781186548,-8.65956056235493E-17));
#6957=DIRECTION('center_axis',(0.,-1.,0.));
#6958=DIRECTION('ref_axis',(0.,0.,-1.));
#6959=DIRECTION('center_axis',(0.,-1.,0.));
#6960=DIRECTION('ref_axis',(1.,0.,0.));
#6961=DIRECTION('center_axis',(0.,1.,0.));
#6962=DIRECTION('ref_axis',(1.,0.,0.));
#6963=DIRECTION('center_axis',(0.,1.,0.));
#6964=DIRECTION('ref_axis',(1.,0.,0.));
#6965=DIRECTION('',(-0.447213595499958,0.894427190999916,-5.47678698264203E-17));
#6966=DIRECTION('center_axis',(0.,-1.,0.));
#6967=DIRECTION('ref_axis',(1.,0.,0.));
#6968=DIRECTION('',(0.,1.,0.));
#8794=CARTESIAN_POINT('',(0.,0.,0.));
#8795=CARTESIAN_POINT('Origin',(0.115470053837925,-0.5,-0.2));
#8796=CARTESIAN_POINT('',(0.23094010767585,-0.5,0.));
#8797=CARTESIAN_POINT('',(0.115470053837925,-0.5,-0.2));
#8798=CARTESIAN_POINT('',(0.23094010767585,-0.5,0.));
#8799=CARTESIAN_POINT('',(0.115470053837925,-0.8,-0.2));
#8800=CARTESIAN_POINT('',(0.115470053837925,-0.5,-0.2));
#8801=CARTESIAN_POINT('',(0.23094010767585,-0.8,0.));
#8802=CARTESIAN_POINT('',(0.23094010767585,-0.8,0.));
#8803=CARTESIAN_POINT('',(0.23094010767585,-0.5,0.));
#8804=CARTESIAN_POINT('Origin',(-0.115470053837925,-0.5,-0.2));
#8805=CARTESIAN_POINT('',(-0.115470053837925,-0.5,-0.2));
#8806=CARTESIAN_POINT('',(0.115470053837925,-0.5,-0.2));
#8807=CARTESIAN_POINT('',(-0.115470053837925,-0.8,-0.2));
#8808=CARTESIAN_POINT('',(-0.115470053837925,-0.5,-0.2));
#8809=CARTESIAN_POINT('',(0.115470053837925,-0.8,-0.2));
#8810=CARTESIAN_POINT('Origin',(-0.23094010767585,-0.5,-2.77555756156289E-17));
#8811=CARTESIAN_POINT('',(-0.23094010767585,-0.5,-2.82820063659975E-17));
#8812=CARTESIAN_POINT('',(-0.115470053837925,-0.5,-0.2));
#8813=CARTESIAN_POINT('',(-0.23094010767585,-0.8,-2.77555756156289E-17));
#8814=CARTESIAN_POINT('',(-0.23094010767585,-0.5,-2.82820063659975E-17));
#8815=CARTESIAN_POINT('',(-0.115470053837925,-0.8,-0.2));
#8816=CARTESIAN_POINT('Origin',(-0.115470053837925,-0.5,0.2));
#8817=CARTESIAN_POINT('',(-0.115470053837925,-0.5,0.2));
#8818=CARTESIAN_POINT('',(-0.23094010767585,-0.5,-2.82820063659975E-17));
#8819=CARTESIAN_POINT('',(-0.115470053837925,-0.8,0.2));
#8820=CARTESIAN_POINT('',(-0.115470053837925,-0.5,0.2));
#8821=CARTESIAN_POINT('',(-0.23094010767585,-0.8,-2.82820063659975E-17));
#8822=CARTESIAN_POINT('Origin',(0.115470053837925,-0.5,0.2));
#8823=CARTESIAN_POINT('',(0.115470053837925,-0.5,0.2));
#8824=CARTESIAN_POINT('',(-0.115470053837925,-0.5,0.2));
#8825=CARTESIAN_POINT('',(0.115470053837925,-0.8,0.2));
#8826=CARTESIAN_POINT('',(0.115470053837925,-0.5,0.2));
#8827=CARTESIAN_POINT('',(-0.115470053837925,-0.8,0.2));
#8828=CARTESIAN_POINT('Origin',(0.23094010767585,-0.5,0.));
#8829=CARTESIAN_POINT('',(0.115470053837925,-0.5,0.2));
#8830=CARTESIAN_POINT('',(0.115470053837925,-0.8,0.2));
#8831=CARTESIAN_POINT('Origin',(0.,-0.5,0.));
#8832=CARTESIAN_POINT('Origin',(0.,-0.8,0.));
#8833=CARTESIAN_POINT('Origin',(0.,-1.4,0.));
#8834=CARTESIAN_POINT('',(-0.24505,-1.4,3.00099698131059E-17));
#8835=CARTESIAN_POINT('Origin',(0.,-1.4,0.));
#8836=CARTESIAN_POINT('Origin',(0.375,0.5,0.));
#8837=CARTESIAN_POINT('',(-0.375,0.5,-4.59242549680257E-17));
#8838=CARTESIAN_POINT('Origin',(0.,0.5,0.));
#8839=CARTESIAN_POINT('Origin',(0.,0.475,0.));
#8840=CARTESIAN_POINT('',(-0.425,0.45,-5.20474889637625E-17));
#8841=CARTESIAN_POINT('Origin',(0.,0.45,0.));
#8842=CARTESIAN_POINT('',(-0.4,0.475,-4.89858719658941E-17));
#8843=CARTESIAN_POINT('Origin',(0.,0.24,0.));
#8844=CARTESIAN_POINT('',(-0.425,0.0299999999999998,-5.20474889637625E-17));
#8845=CARTESIAN_POINT('Origin',(0.,0.0299999999999998,0.));
#8846=CARTESIAN_POINT('',(-0.425,0.24,-5.20474889637625E-17));
#8847=CARTESIAN_POINT('Origin',(0.,0.0150000000000001,0.));
#8848=CARTESIAN_POINT('',(-0.395,4.85722573273506E-17,-4.83735485663204E-17));
#8849=CARTESIAN_POINT('Origin',(0.,0.,0.));
#8850=CARTESIAN_POINT('',(-0.41,0.0150000000000001,-5.02105187650415E-17));
#8851=CARTESIAN_POINT('Origin',(0.27,0.,0.));
#8852=CARTESIAN_POINT('',(-0.27,0.,-3.30654635769785E-17));
#8853=CARTESIAN_POINT('Origin',(0.,0.,0.));
#8854=CARTESIAN_POINT('Origin',(0.,-0.02,0.));
#8855=CARTESIAN_POINT('',(-0.24505,-0.0498999999999999,3.00099698131059E-17));
#8856=CARTESIAN_POINT('Origin',(0.,-0.0498999999999999,0.));
#8857=CARTESIAN_POINT('',(-0.26,-0.02,-3.18408167778312E-17));
#8858=CARTESIAN_POINT('Origin',(0.,-0.995,0.));
#8859=CARTESIAN_POINT('',(-0.24505,-0.995,-3.00099698131059E-17));
#11216=UNCERTAINTY_MEASURE_WITH_UNIT(LENGTH_MEASURE(0.001),#11259,
'DISTANCE_ACCURACY_VALUE',
'Maximum model space distance between geometric entities at asserted c
onnectivities');
#11228=UNCERTAINTY_MEASURE_WITH_UNIT(LENGTH_MEASURE(0.001),#11259,
'DISTANCE_ACCURACY_VALUE',
'Maximum model space distance between geometric entities at asserted c
onnectivities');
#11246=(
GEOMETRIC_REPRESENTATION_CONTEXT(3)
GLOBAL_UNCERTAINTY_ASSIGNED_CONTEXT((#11216))
GLOBAL_UNIT_ASSIGNED_CONTEXT((#11259,#11261,#11262))
REPRESENTATION_CONTEXT('','3D')
);
#11258=(
GEOMETRIC_REPRESENTATION_CONTEXT(3)
GLOBAL_UNCERTAINTY_ASSIGNED_CONTEXT((#11228))
GLOBAL_UNIT_ASSIGNED_CONTEXT((#11259,#11261,#11262))
REPRESENTATION_CONTEXT('','3D')
);
#11259=(
LENGTH_UNIT()
NAMED_UNIT(*)
SI_UNIT(.CENTI.,.METRE.)
);
#11261=(
NAMED_UNIT(*)
PLANE_ANGLE_UNIT()
SI_UNIT($,.RADIAN.)
);
#11262=(
NAMED_UNIT(*)
SI_UNIT($,.STERADIAN.)
SOLID_ANGLE_UNIT()
);
#11280=SHAPE_DEFINITION_REPRESENTATION(#11314,#11376);
#11314=PRODUCT_DEFINITION_SHAPE('',$,#11406);
#11376=SHAPE_REPRESENTATION('',(#5814),#11246);
#11388=PRODUCT_DEFINITION_CONTEXT('part definition',#11477,'design');
#11406=PRODUCT_DEFINITION('M5x14 Cap Screw','M5x14 Cap Screw',#11435,#11388);
#11435=PRODUCT_DEFINITION_FORMATION('',$,#11496);
#11477=APPLICATION_CONTEXT(
'Core Data for Automotive Mechanical Design Process');
#11478=PRODUCT_CONTEXT('part definition',#11477,'mechanical');
#11496=PRODUCT('M5x14 Cap Screw','M5x14 Cap Screw','M5x14 Cap Screw',(#11478));
#11585=COLOUR_RGB('Black',0.12,0.14,0.17);
#11586=FILL_AREA_STYLE_COLOUR('',#11585);
#11587=FILL_AREA_STYLE('',(#11586));
#11588=SURFACE_STYLE_FILL_AREA(#11587);
#11589=SURFACE_SIDE_STYLE('',(#11588));
#11590=SURFACE_STYLE_USAGE(.BOTH.,#11589);
#11591=PRESENTATION_STYLE_ASSIGNMENT((#11590));
ENDSEC;
END-ISO-10303-21;
